ISO-10303-21;
HEADER;
/* Generated by software containing ST-Developer
 * from STEP Tools, Inc. (www.steptools.com) 
 */

FILE_DESCRIPTION(
/* description */ (''),
/* implementation_level */ '2;1');

FILE_NAME(
/* name */ 'FLYWHEEL.step',
/* time_stamp */ '2026-10-06T01:16:10-07:00',
/* author */ (''),
/* organization */ (''),
/* preprocessor_version */ 'ST-DEVELOPER v20.2',
/* originating_system */ 'Autodesk Translation Framework v15.15.0.0',
/* authorisation */ '');

FILE_SCHEMA (('AUTOMOTIVE_DESIGN { 1 0 10303 214 3 1 1 }'));
ENDSEC;

DATA;
#10=MECHANICAL_DESIGN_GEOMETRIC_PRESENTATION_REPRESENTATION('',(#306),#17113);
#170=B_SPLINE_CURVE_WITH_KNOTS('',3,(#10460,#10461,#10462,#10463,#10464,
#10465,#10466,#10467,#10468,#10469,#10470,#10471,#10472,#10473,#10474,#10475,
#10476,#10477),.UNSPECIFIED.,.F.,.F.,(4,2,2,2,2,2,2,2,4),(-0.567632662698663,
-0.520333247919949,-0.473033833141235,-0.425727804136839,-0.378421775132442,
-0.331115746128045,-0.283809717123649,-0.236510302344935,-0.189210887566221),
 .UNSPECIFIED.);
#171=B_SPLINE_CURVE_WITH_KNOTS('',3,(#10478,#10479,#10480,#10481,#10482,
#10483,#10484,#10485,#10486,#10487,#10488,#10489,#10490,#10491,#10492,#10493,
#10494,#10495,#10496),.UNSPECIFIED.,.F.,.F.,(4,2,2,2,3,2,2,2,4),(-0.189210887566221,
-0.141911472787507,-0.0946120580087934,-0.0473060290043967,0.,0.0473060290043967,
0.0946120580087935,0.141911472787507,0.189210887566221),.UNSPECIFIED.);
#172=B_SPLINE_CURVE_WITH_KNOTS('',3,(#10498,#10499,#10500,#10501,#10502,
#10503,#10504,#10505,#10506,#10507,#10508,#10509,#10510,#10511,#10512,#10513,
#10514,#10515,#10516,#10517,#10518,#10519,#10520,#10521,#10522,#10523,#10524,
#10525,#10526,#10527,#10528,#10529,#10530,#10531),.UNSPECIFIED.,.T.,.F.,
(4,2,2,2,2,2,2,2,2,2,2,2,2,2,2,2,4),(-0.756843550264884,-0.709537521260487,
-0.662231492256091,-0.614932077477377,-0.567632662698663,-0.520333247919949,
-0.473033833141235,-0.425727804136839,-0.378421775132442,-0.331115746128045,
-0.283809717123649,-0.236510302344935,-0.189210887566221,-0.141911472787507,
-0.0946120580087934,-0.0473060290043967,0.),.UNSPECIFIED.);
#173=B_SPLINE_CURVE_WITH_KNOTS('',3,(#10598,#10599,#10600,#10601,#10602,
#10603,#10604,#10605,#10606,#10607,#10608,#10609,#10610,#10611,#10612,#10613,
#10614,#10615,#10616,#10617,#10618,#10619,#10620,#10621,#10622,#10623,#10624,
#10625,#10626,#10627,#10628,#10629,#10630,#10631),.UNSPECIFIED.,.T.,.F.,
(4,2,2,2,2,2,2,2,2,2,2,2,2,2,2,2,4),(0.,0.0481144001101842,0.0962288002203683,
0.144212038136127,0.192195276051885,0.240178513967643,0.288161751883402,
0.336276151993586,0.38439055210377,0.432504952213954,0.480619352324138,
0.528602590239897,0.576585828155655,0.624569066071413,0.672552303987172,
0.720666704097356,0.76878110420754),.UNSPECIFIED.);
#174=B_SPLINE_CURVE_WITH_KNOTS('',3,(#10634,#10635,#10636,#10637,#10638,
#10639,#10640,#10641,#10642,#10643,#10644,#10645,#10646,#10647,#10648,#10649,
#10650,#10651),.UNSPECIFIED.,.F.,.F.,(4,2,2,2,2,2,2,2,4),(0.192195276051885,
0.240178513967643,0.288161751883402,0.336276151993586,0.38439055210377,
0.432504952213954,0.480619352324138,0.528602590239897,0.576585828155655),
 .UNSPECIFIED.);
#175=B_SPLINE_CURVE_WITH_KNOTS('',3,(#10652,#10653,#10654,#10655,#10656,
#10657,#10658,#10659,#10660,#10661,#10662,#10663,#10664,#10665,#10666,#10667,
#10668,#10669,#10670),.UNSPECIFIED.,.F.,.F.,(4,2,2,2,3,2,2,2,4),(0.576585828155655,
0.624569066071413,0.672552303987172,0.720666704097356,0.76878110420754,
0.816895504317724,0.865009904427908,0.912993142343667,0.960976380259425),
 .UNSPECIFIED.);
#268=SHAPE_REPRESENTATION_RELATIONSHIP('SRR','None',#17191,#284);
#284=ADVANCED_BREP_SHAPE_REPRESENTATION('',(#334),#17098);
#306=STYLED_ITEM('',(#17298),#334);
#334=MANIFOLD_SOLID_BREP('Body1',#6020);
#415=CYLINDRICAL_SURFACE('',#6562,5.);
#416=CYLINDRICAL_SURFACE('',#6574,35.);
#417=CYLINDRICAL_SURFACE('',#6578,40.);
#418=CYLINDRICAL_SURFACE('',#6582,35.);
#419=CYLINDRICAL_SURFACE('',#6594,5.);
#420=CYLINDRICAL_SURFACE('',#6598,2.5);
#421=CYLINDRICAL_SURFACE('',#6599,1.25);
#422=CYLINDRICAL_SURFACE('',#6600,1.25);
#423=CYLINDRICAL_SURFACE('',#6601,12.5);
#424=CYLINDRICAL_SURFACE('',#6602,12.5);
#425=CYLINDRICAL_SURFACE('',#6603,12.5);
#426=CYLINDRICAL_SURFACE('',#6604,12.5);
#427=CYLINDRICAL_SURFACE('',#6605,6.);
#428=CYLINDRICAL_SURFACE('',#6606,6.);
#429=CYLINDRICAL_SURFACE('',#6607,6.);
#430=CYLINDRICAL_SURFACE('',#6608,6.);
#551=FACE_BOUND('',#1585,.T.);
#552=FACE_BOUND('',#1587,.T.);
#553=FACE_BOUND('',#1588,.T.);
#554=FACE_BOUND('',#1590,.T.);
#555=FACE_BOUND('',#1591,.T.);
#556=FACE_BOUND('',#1592,.T.);
#557=FACE_BOUND('',#1593,.T.);
#558=FACE_BOUND('',#1594,.T.);
#559=FACE_BOUND('',#1595,.T.);
#560=FACE_BOUND('',#1596,.T.);
#561=FACE_BOUND('',#1597,.T.);
#562=FACE_BOUND('',#1598,.T.);
#563=FACE_BOUND('',#1601,.T.);
#564=FACE_BOUND('',#1604,.T.);
#565=FACE_BOUND('',#1607,.T.);
#566=FACE_BOUND('',#1608,.T.);
#567=FACE_BOUND('',#1609,.T.);
#568=FACE_BOUND('',#1610,.T.);
#569=FACE_BOUND('',#1611,.T.);
#570=FACE_BOUND('',#1612,.T.);
#571=FACE_BOUND('',#1613,.T.);
#572=FACE_BOUND('',#1614,.T.);
#573=FACE_BOUND('',#1615,.T.);
#574=FACE_BOUND('',#1618,.T.);
#575=FACE_BOUND('',#1620,.T.);
#576=FACE_BOUND('',#1621,.T.);
#808=CIRCLE('',#6560,5.);
#809=CIRCLE('',#6561,2.5);
#810=CIRCLE('',#6563,5.);
#811=CIRCLE('',#6565,35.);
#812=CIRCLE('',#6566,12.5);
#813=CIRCLE('',#6567,12.5);
#814=CIRCLE('',#6568,12.5);
#815=CIRCLE('',#6569,12.5);
#816=CIRCLE('',#6570,6.);
#817=CIRCLE('',#6571,6.);
#818=CIRCLE('',#6572,6.);
#819=CIRCLE('',#6573,6.);
#820=CIRCLE('',#6575,35.);
#821=CIRCLE('',#6577,40.);
#822=CIRCLE('',#6579,40.);
#823=CIRCLE('',#6581,35.);
#824=CIRCLE('',#6583,35.);
#825=CIRCLE('',#6585,5.);
#826=CIRCLE('',#6586,12.5);
#827=CIRCLE('',#6587,12.5);
#828=CIRCLE('',#6588,12.5);
#829=CIRCLE('',#6589,12.5);
#830=CIRCLE('',#6590,6.);
#831=CIRCLE('',#6591,6.);
#832=CIRCLE('',#6592,6.);
#833=CIRCLE('',#6593,6.);
#834=CIRCLE('',#6595,5.);
#835=CIRCLE('',#6597,2.5);
#1177=FACE_OUTER_BOUND('',#1584,.T.);
#1178=FACE_OUTER_BOUND('',#1586,.T.);
#1179=FACE_OUTER_BOUND('',#1589,.T.);
#1180=FACE_OUTER_BOUND('',#1599,.T.);
#1181=FACE_OUTER_BOUND('',#1600,.T.);
#1182=FACE_OUTER_BOUND('',#1602,.T.);
#1183=FACE_OUTER_BOUND('',#1603,.T.);
#1184=FACE_OUTER_BOUND('',#1605,.T.);
#1185=FACE_OUTER_BOUND('',#1606,.T.);
#1186=FACE_OUTER_BOUND('',#1616,.T.);
#1187=FACE_OUTER_BOUND('',#1617,.T.);
#1188=FACE_OUTER_BOUND('',#1619,.T.);
#1189=FACE_OUTER_BOUND('',#1622,.T.);
#1190=FACE_OUTER_BOUND('',#1623,.T.);
#1191=FACE_OUTER_BOUND('',#1624,.T.);
#1192=FACE_OUTER_BOUND('',#1625,.T.);
#1193=FACE_OUTER_BOUND('',#1626,.T.);
#1194=FACE_OUTER_BOUND('',#1627,.T.);
#1195=FACE_OUTER_BOUND('',#1628,.T.);
#1196=FACE_OUTER_BOUND('',#1629,.T.);
#1197=FACE_OUTER_BOUND('',#1630,.T.);
#1198=FACE_OUTER_BOUND('',#1631,.T.);
#1584=EDGE_LOOP('',(#4688));
#1585=EDGE_LOOP('',(#4689));
#1586=EDGE_LOOP('',(#4690,#4691,#4692,#4693));
#1587=EDGE_LOOP('',(#4694,#4695));
#1588=EDGE_LOOP('',(#4696));
#1589=EDGE_LOOP('',(#4697));
#1590=EDGE_LOOP('',(#4698));
#1591=EDGE_LOOP('',(#4699));
#1592=EDGE_LOOP('',(#4700));
#1593=EDGE_LOOP('',(#4701));
#1594=EDGE_LOOP('',(#4702));
#1595=EDGE_LOOP('',(#4703));
#1596=EDGE_LOOP('',(#4704));
#1597=EDGE_LOOP('',(#4705));
#1598=EDGE_LOOP('',(#4706));
#1599=EDGE_LOOP('',(#4707,#4708,#4709,#4710));
#1600=EDGE_LOOP('',(#4711));
#1601=EDGE_LOOP('',(#4712));
#1602=EDGE_LOOP('',(#4713,#4714,#4715,#4716));
#1603=EDGE_LOOP('',(#4717));
#1604=EDGE_LOOP('',(#4718));
#1605=EDGE_LOOP('',(#4719,#4720,#4721,#4722));
#1606=EDGE_LOOP('',(#4723));
#1607=EDGE_LOOP('',(#4724));
#1608=EDGE_LOOP('',(#4725));
#1609=EDGE_LOOP('',(#4726));
#1610=EDGE_LOOP('',(#4727));
#1611=EDGE_LOOP('',(#4728));
#1612=EDGE_LOOP('',(#4729));
#1613=EDGE_LOOP('',(#4730));
#1614=EDGE_LOOP('',(#4731));
#1615=EDGE_LOOP('',(#4732));
#1616=EDGE_LOOP('',(#4733,#4734,#4735,#4736));
#1617=EDGE_LOOP('',(#4737));
#1618=EDGE_LOOP('',(#4738));
#1619=EDGE_LOOP('',(#4739,#4740,#4741,#4742));
#1620=EDGE_LOOP('',(#4743));
#1621=EDGE_LOOP('',(#4744,#4745));
#1622=EDGE_LOOP('',(#4746,#4747,#4748,#4749,#4750));
#1623=EDGE_LOOP('',(#4751,#4752,#4753,#4754,#4755));
#1624=EDGE_LOOP('',(#4756,#4757,#4758,#4759));
#1625=EDGE_LOOP('',(#4760,#4761,#4762,#4763));
#1626=EDGE_LOOP('',(#4764,#4765,#4766,#4767));
#1627=EDGE_LOOP('',(#4768,#4769,#4770,#4771));
#1628=EDGE_LOOP('',(#4772,#4773,#4774,#4775));
#1629=EDGE_LOOP('',(#4776,#4777,#4778,#4779));
#1630=EDGE_LOOP('',(#4780,#4781,#4782,#4783));
#1631=EDGE_LOOP('',(#4784,#4785,#4786,#4787));
#2054=LINE('',#10456,#2415);
#2055=LINE('',#10553,#2416);
#2056=LINE('',#10560,#2417);
#2057=LINE('',#10567,#2418);
#2058=LINE('',#10590,#2419);
#2059=LINE('',#10596,#2420);
#2060=LINE('',#10672,#2421);
#2061=LINE('',#10674,#2422);
#2062=LINE('',#10676,#2423);
#2063=LINE('',#10678,#2424);
#2064=LINE('',#10680,#2425);
#2065=LINE('',#10682,#2426);
#2066=LINE('',#10684,#2427);
#2067=LINE('',#10686,#2428);
#2068=LINE('',#10688,#2429);
#2069=LINE('',#10690,#2430);
#2415=VECTOR('',#7880,5.);
#2416=VECTOR('',#7905,35.);
#2417=VECTOR('',#7914,40.);
#2418=VECTOR('',#7923,35.);
#2419=VECTOR('',#7948,5.);
#2420=VECTOR('',#7957,2.5);
#2421=VECTOR('',#7960,1.25);
#2422=VECTOR('',#7963,1.25);
#2423=VECTOR('',#7966,12.5);
#2424=VECTOR('',#7969,12.5);
#2425=VECTOR('',#7972,12.5);
#2426=VECTOR('',#7975,12.5);
#2427=VECTOR('',#7978,6.);
#2428=VECTOR('',#7981,6.);
#2429=VECTOR('',#7984,6.);
#2430=VECTOR('',#7987,6.);
#2824=VERTEX_POINT('',#10450);
#2825=VERTEX_POINT('',#10452);
#2826=VERTEX_POINT('',#10455);
#2827=VERTEX_POINT('',#10458);
#2828=VERTEX_POINT('',#10459);
#2829=VERTEX_POINT('',#10497);
#2830=VERTEX_POINT('',#10533);
#2831=VERTEX_POINT('',#10535);
#2832=VERTEX_POINT('',#10537);
#2833=VERTEX_POINT('',#10539);
#2834=VERTEX_POINT('',#10541);
#2835=VERTEX_POINT('',#10543);
#2836=VERTEX_POINT('',#10545);
#2837=VERTEX_POINT('',#10547);
#2838=VERTEX_POINT('',#10549);
#2839=VERTEX_POINT('',#10552);
#2840=VERTEX_POINT('',#10556);
#2841=VERTEX_POINT('',#10559);
#2842=VERTEX_POINT('',#10563);
#2843=VERTEX_POINT('',#10566);
#2844=VERTEX_POINT('',#10570);
#2845=VERTEX_POINT('',#10572);
#2846=VERTEX_POINT('',#10574);
#2847=VERTEX_POINT('',#10576);
#2848=VERTEX_POINT('',#10578);
#2849=VERTEX_POINT('',#10580);
#2850=VERTEX_POINT('',#10582);
#2851=VERTEX_POINT('',#10584);
#2852=VERTEX_POINT('',#10586);
#2853=VERTEX_POINT('',#10589);
#2854=VERTEX_POINT('',#10593);
#2855=VERTEX_POINT('',#10597);
#2856=VERTEX_POINT('',#10632);
#2857=VERTEX_POINT('',#10633);
#3496=EDGE_CURVE('',#2824,#2824,#808,.T.);
#3497=EDGE_CURVE('',#2825,#2825,#809,.T.);
#3498=EDGE_CURVE('',#2824,#2826,#2054,.T.);
#3499=EDGE_CURVE('',#2826,#2826,#810,.T.);
#3500=EDGE_CURVE('',#2827,#2828,#170,.T.);
#3501=EDGE_CURVE('',#2828,#2827,#171,.T.);
#3502=EDGE_CURVE('',#2829,#2829,#172,.T.);
#3503=EDGE_CURVE('',#2830,#2830,#811,.T.);
#3504=EDGE_CURVE('',#2831,#2831,#812,.T.);
#3505=EDGE_CURVE('',#2832,#2832,#813,.T.);
#3506=EDGE_CURVE('',#2833,#2833,#814,.T.);
#3507=EDGE_CURVE('',#2834,#2834,#815,.T.);
#3508=EDGE_CURVE('',#2835,#2835,#816,.T.);
#3509=EDGE_CURVE('',#2836,#2836,#817,.T.);
#3510=EDGE_CURVE('',#2837,#2837,#818,.T.);
#3511=EDGE_CURVE('',#2838,#2838,#819,.T.);
#3512=EDGE_CURVE('',#2830,#2839,#2055,.T.);
#3513=EDGE_CURVE('',#2839,#2839,#820,.T.);
#3514=EDGE_CURVE('',#2840,#2840,#821,.T.);
#3515=EDGE_CURVE('',#2840,#2841,#2056,.T.);
#3516=EDGE_CURVE('',#2841,#2841,#822,.T.);
#3517=EDGE_CURVE('',#2842,#2842,#823,.T.);
#3518=EDGE_CURVE('',#2842,#2843,#2057,.T.);
#3519=EDGE_CURVE('',#2843,#2843,#824,.T.);
#3520=EDGE_CURVE('',#2844,#2844,#825,.T.);
#3521=EDGE_CURVE('',#2845,#2845,#826,.T.);
#3522=EDGE_CURVE('',#2846,#2846,#827,.T.);
#3523=EDGE_CURVE('',#2847,#2847,#828,.T.);
#3524=EDGE_CURVE('',#2848,#2848,#829,.T.);
#3525=EDGE_CURVE('',#2849,#2849,#830,.T.);
#3526=EDGE_CURVE('',#2850,#2850,#831,.T.);
#3527=EDGE_CURVE('',#2851,#2851,#832,.T.);
#3528=EDGE_CURVE('',#2852,#2852,#833,.T.);
#3529=EDGE_CURVE('',#2844,#2853,#2058,.T.);
#3530=EDGE_CURVE('',#2853,#2853,#834,.T.);
#3531=EDGE_CURVE('',#2854,#2854,#835,.T.);
#3532=EDGE_CURVE('',#2854,#2825,#2059,.T.);
#3533=EDGE_CURVE('',#2855,#2855,#173,.T.);
#3534=EDGE_CURVE('',#2856,#2857,#174,.T.);
#3535=EDGE_CURVE('',#2857,#2856,#175,.T.);
#3536=EDGE_CURVE('',#2857,#2829,#2060,.T.);
#3537=EDGE_CURVE('',#2828,#2855,#2061,.T.);
#3538=EDGE_CURVE('',#2831,#2845,#2062,.T.);
#3539=EDGE_CURVE('',#2832,#2846,#2063,.T.);
#3540=EDGE_CURVE('',#2833,#2847,#2064,.T.);
#3541=EDGE_CURVE('',#2834,#2848,#2065,.T.);
#3542=EDGE_CURVE('',#2835,#2849,#2066,.T.);
#3543=EDGE_CURVE('',#2836,#2850,#2067,.T.);
#3544=EDGE_CURVE('',#2837,#2851,#2068,.T.);
#3545=EDGE_CURVE('',#2838,#2852,#2069,.T.);
#4688=ORIENTED_EDGE('',*,*,#3496,.T.);
#4689=ORIENTED_EDGE('',*,*,#3497,.T.);
#4690=ORIENTED_EDGE('',*,*,#3496,.F.);
#4691=ORIENTED_EDGE('',*,*,#3498,.T.);
#4692=ORIENTED_EDGE('',*,*,#3499,.T.);
#4693=ORIENTED_EDGE('',*,*,#3498,.F.);
#4694=ORIENTED_EDGE('',*,*,#3500,.T.);
#4695=ORIENTED_EDGE('',*,*,#3501,.T.);
#4696=ORIENTED_EDGE('',*,*,#3502,.T.);
#4697=ORIENTED_EDGE('',*,*,#3503,.T.);
#4698=ORIENTED_EDGE('',*,*,#3499,.F.);
#4699=ORIENTED_EDGE('',*,*,#3504,.T.);
#4700=ORIENTED_EDGE('',*,*,#3505,.T.);
#4701=ORIENTED_EDGE('',*,*,#3506,.T.);
#4702=ORIENTED_EDGE('',*,*,#3507,.T.);
#4703=ORIENTED_EDGE('',*,*,#3508,.T.);
#4704=ORIENTED_EDGE('',*,*,#3509,.T.);
#4705=ORIENTED_EDGE('',*,*,#3510,.T.);
#4706=ORIENTED_EDGE('',*,*,#3511,.T.);
#4707=ORIENTED_EDGE('',*,*,#3503,.F.);
#4708=ORIENTED_EDGE('',*,*,#3512,.T.);
#4709=ORIENTED_EDGE('',*,*,#3513,.T.);
#4710=ORIENTED_EDGE('',*,*,#3512,.F.);
#4711=ORIENTED_EDGE('',*,*,#3514,.T.);
#4712=ORIENTED_EDGE('',*,*,#3513,.F.);
#4713=ORIENTED_EDGE('',*,*,#3514,.F.);
#4714=ORIENTED_EDGE('',*,*,#3515,.T.);
#4715=ORIENTED_EDGE('',*,*,#3516,.T.);
#4716=ORIENTED_EDGE('',*,*,#3515,.F.);
#4717=ORIENTED_EDGE('',*,*,#3516,.F.);
#4718=ORIENTED_EDGE('',*,*,#3517,.T.);
#4719=ORIENTED_EDGE('',*,*,#3517,.F.);
#4720=ORIENTED_EDGE('',*,*,#3518,.T.);
#4721=ORIENTED_EDGE('',*,*,#3519,.T.);
#4722=ORIENTED_EDGE('',*,*,#3518,.F.);
#4723=ORIENTED_EDGE('',*,*,#3519,.F.);
#4724=ORIENTED_EDGE('',*,*,#3520,.T.);
#4725=ORIENTED_EDGE('',*,*,#3521,.F.);
#4726=ORIENTED_EDGE('',*,*,#3522,.F.);
#4727=ORIENTED_EDGE('',*,*,#3523,.F.);
#4728=ORIENTED_EDGE('',*,*,#3524,.F.);
#4729=ORIENTED_EDGE('',*,*,#3525,.F.);
#4730=ORIENTED_EDGE('',*,*,#3526,.F.);
#4731=ORIENTED_EDGE('',*,*,#3527,.F.);
#4732=ORIENTED_EDGE('',*,*,#3528,.F.);
#4733=ORIENTED_EDGE('',*,*,#3520,.F.);
#4734=ORIENTED_EDGE('',*,*,#3529,.T.);
#4735=ORIENTED_EDGE('',*,*,#3530,.T.);
#4736=ORIENTED_EDGE('',*,*,#3529,.F.);
#4737=ORIENTED_EDGE('',*,*,#3530,.F.);
#4738=ORIENTED_EDGE('',*,*,#3531,.T.);
#4739=ORIENTED_EDGE('',*,*,#3531,.F.);
#4740=ORIENTED_EDGE('',*,*,#3532,.T.);
#4741=ORIENTED_EDGE('',*,*,#3497,.F.);
#4742=ORIENTED_EDGE('',*,*,#3532,.F.);
#4743=ORIENTED_EDGE('',*,*,#3533,.T.);
#4744=ORIENTED_EDGE('',*,*,#3534,.T.);
#4745=ORIENTED_EDGE('',*,*,#3535,.T.);
#4746=ORIENTED_EDGE('',*,*,#3534,.F.);
#4747=ORIENTED_EDGE('',*,*,#3535,.F.);
#4748=ORIENTED_EDGE('',*,*,#3536,.T.);
#4749=ORIENTED_EDGE('',*,*,#3502,.F.);
#4750=ORIENTED_EDGE('',*,*,#3536,.F.);
#4751=ORIENTED_EDGE('',*,*,#3500,.F.);
#4752=ORIENTED_EDGE('',*,*,#3501,.F.);
#4753=ORIENTED_EDGE('',*,*,#3537,.T.);
#4754=ORIENTED_EDGE('',*,*,#3533,.F.);
#4755=ORIENTED_EDGE('',*,*,#3537,.F.);
#4756=ORIENTED_EDGE('',*,*,#3504,.F.);
#4757=ORIENTED_EDGE('',*,*,#3538,.T.);
#4758=ORIENTED_EDGE('',*,*,#3521,.T.);
#4759=ORIENTED_EDGE('',*,*,#3538,.F.);
#4760=ORIENTED_EDGE('',*,*,#3505,.F.);
#4761=ORIENTED_EDGE('',*,*,#3539,.T.);
#4762=ORIENTED_EDGE('',*,*,#3522,.T.);
#4763=ORIENTED_EDGE('',*,*,#3539,.F.);
#4764=ORIENTED_EDGE('',*,*,#3506,.F.);
#4765=ORIENTED_EDGE('',*,*,#3540,.T.);
#4766=ORIENTED_EDGE('',*,*,#3523,.T.);
#4767=ORIENTED_EDGE('',*,*,#3540,.F.);
#4768=ORIENTED_EDGE('',*,*,#3507,.F.);
#4769=ORIENTED_EDGE('',*,*,#3541,.T.);
#4770=ORIENTED_EDGE('',*,*,#3524,.T.);
#4771=ORIENTED_EDGE('',*,*,#3541,.F.);
#4772=ORIENTED_EDGE('',*,*,#3508,.F.);
#4773=ORIENTED_EDGE('',*,*,#3542,.T.);
#4774=ORIENTED_EDGE('',*,*,#3525,.T.);
#4775=ORIENTED_EDGE('',*,*,#3542,.F.);
#4776=ORIENTED_EDGE('',*,*,#3509,.F.);
#4777=ORIENTED_EDGE('',*,*,#3543,.T.);
#4778=ORIENTED_EDGE('',*,*,#3526,.T.);
#4779=ORIENTED_EDGE('',*,*,#3543,.F.);
#4780=ORIENTED_EDGE('',*,*,#3510,.F.);
#4781=ORIENTED_EDGE('',*,*,#3544,.T.);
#4782=ORIENTED_EDGE('',*,*,#3527,.T.);
#4783=ORIENTED_EDGE('',*,*,#3544,.F.);
#4784=ORIENTED_EDGE('',*,*,#3511,.F.);
#4785=ORIENTED_EDGE('',*,*,#3545,.T.);
#4786=ORIENTED_EDGE('',*,*,#3528,.T.);
#4787=ORIENTED_EDGE('',*,*,#3545,.F.);
#5571=PLANE('',#6559);
#5572=PLANE('',#6564);
#5573=PLANE('',#6576);
#5574=PLANE('',#6580);
#5575=PLANE('',#6584);
#5576=PLANE('',#6596);
#5825=ADVANCED_FACE('',(#1177,#551),#5571,.T.);
#5826=ADVANCED_FACE('',(#1178,#552,#553),#415,.T.);
#5827=ADVANCED_FACE('',(#1179,#554,#555,#556,#557,#558,#559,#560,#561,#562),
#5572,.T.);
#5828=ADVANCED_FACE('',(#1180),#416,.F.);
#5829=ADVANCED_FACE('',(#1181,#563),#5573,.T.);
#5830=ADVANCED_FACE('',(#1182),#417,.T.);
#5831=ADVANCED_FACE('',(#1183,#564),#5574,.F.);
#5832=ADVANCED_FACE('',(#1184),#418,.F.);
#5833=ADVANCED_FACE('',(#1185,#565,#566,#567,#568,#569,#570,#571,#572,#573),
#5575,.F.);
#5834=ADVANCED_FACE('',(#1186),#419,.T.);
#5835=ADVANCED_FACE('',(#1187,#574),#5576,.F.);
#5836=ADVANCED_FACE('',(#1188,#575,#576),#420,.F.);
#5837=ADVANCED_FACE('',(#1189),#421,.F.);
#5838=ADVANCED_FACE('',(#1190),#422,.F.);
#5839=ADVANCED_FACE('',(#1191),#423,.F.);
#5840=ADVANCED_FACE('',(#1192),#424,.F.);
#5841=ADVANCED_FACE('',(#1193),#425,.F.);
#5842=ADVANCED_FACE('',(#1194),#426,.F.);
#5843=ADVANCED_FACE('',(#1195),#427,.F.);
#5844=ADVANCED_FACE('',(#1196),#428,.F.);
#5845=ADVANCED_FACE('',(#1197),#429,.F.);
#5846=ADVANCED_FACE('',(#1198),#430,.F.);
#6020=CLOSED_SHELL('',(#5825,#5826,#5827,#5828,#5829,#5830,#5831,#5832,
#5833,#5834,#5835,#5836,#5837,#5838,#5839,#5840,#5841,#5842,#5843,#5844,
#5845,#5846));
#6558=AXIS2_PLACEMENT_3D('',#10448,#7870,#7871);
#6559=AXIS2_PLACEMENT_3D('',#10449,#7872,#7873);
#6560=AXIS2_PLACEMENT_3D('',#10451,#7874,#7875);
#6561=AXIS2_PLACEMENT_3D('',#10453,#7876,#7877);
#6562=AXIS2_PLACEMENT_3D('',#10454,#7878,#7879);
#6563=AXIS2_PLACEMENT_3D('',#10457,#7881,#7882);
#6564=AXIS2_PLACEMENT_3D('',#10532,#7883,#7884);
#6565=AXIS2_PLACEMENT_3D('',#10534,#7885,#7886);
#6566=AXIS2_PLACEMENT_3D('',#10536,#7887,#7888);
#6567=AXIS2_PLACEMENT_3D('',#10538,#7889,#7890);
#6568=AXIS2_PLACEMENT_3D('',#10540,#7891,#7892);
#6569=AXIS2_PLACEMENT_3D('',#10542,#7893,#7894);
#6570=AXIS2_PLACEMENT_3D('',#10544,#7895,#7896);
#6571=AXIS2_PLACEMENT_3D('',#10546,#7897,#7898);
#6572=AXIS2_PLACEMENT_3D('',#10548,#7899,#7900);
#6573=AXIS2_PLACEMENT_3D('',#10550,#7901,#7902);
#6574=AXIS2_PLACEMENT_3D('',#10551,#7903,#7904);
#6575=AXIS2_PLACEMENT_3D('',#10554,#7906,#7907);
#6576=AXIS2_PLACEMENT_3D('',#10555,#7908,#7909);
#6577=AXIS2_PLACEMENT_3D('',#10557,#7910,#7911);
#6578=AXIS2_PLACEMENT_3D('',#10558,#7912,#7913);
#6579=AXIS2_PLACEMENT_3D('',#10561,#7915,#7916);
#6580=AXIS2_PLACEMENT_3D('',#10562,#7917,#7918);
#6581=AXIS2_PLACEMENT_3D('',#10564,#7919,#7920);
#6582=AXIS2_PLACEMENT_3D('',#10565,#7921,#7922);
#6583=AXIS2_PLACEMENT_3D('',#10568,#7924,#7925);
#6584=AXIS2_PLACEMENT_3D('',#10569,#7926,#7927);
#6585=AXIS2_PLACEMENT_3D('',#10571,#7928,#7929);
#6586=AXIS2_PLACEMENT_3D('',#10573,#7930,#7931);
#6587=AXIS2_PLACEMENT_3D('',#10575,#7932,#7933);
#6588=AXIS2_PLACEMENT_3D('',#10577,#7934,#7935);
#6589=AXIS2_PLACEMENT_3D('',#10579,#7936,#7937);
#6590=AXIS2_PLACEMENT_3D('',#10581,#7938,#7939);
#6591=AXIS2_PLACEMENT_3D('',#10583,#7940,#7941);
#6592=AXIS2_PLACEMENT_3D('',#10585,#7942,#7943);
#6593=AXIS2_PLACEMENT_3D('',#10587,#7944,#7945);
#6594=AXIS2_PLACEMENT_3D('',#10588,#7946,#7947);
#6595=AXIS2_PLACEMENT_3D('',#10591,#7949,#7950);
#6596=AXIS2_PLACEMENT_3D('',#10592,#7951,#7952);
#6597=AXIS2_PLACEMENT_3D('',#10594,#7953,#7954);
#6598=AXIS2_PLACEMENT_3D('',#10595,#7955,#7956);
#6599=AXIS2_PLACEMENT_3D('',#10671,#7958,#7959);
#6600=AXIS2_PLACEMENT_3D('',#10673,#7961,#7962);
#6601=AXIS2_PLACEMENT_3D('',#10675,#7964,#7965);
#6602=AXIS2_PLACEMENT_3D('',#10677,#7967,#7968);
#6603=AXIS2_PLACEMENT_3D('',#10679,#7970,#7971);
#6604=AXIS2_PLACEMENT_3D('',#10681,#7973,#7974);
#6605=AXIS2_PLACEMENT_3D('',#10683,#7976,#7977);
#6606=AXIS2_PLACEMENT_3D('',#10685,#7979,#7980);
#6607=AXIS2_PLACEMENT_3D('',#10687,#7982,#7983);
#6608=AXIS2_PLACEMENT_3D('',#10689,#7985,#7986);
#7870=DIRECTION('axis',(0.,0.,1.));
#7871=DIRECTION('refdir',(1.,0.,0.));
#7872=DIRECTION('center_axis',(0.,-1.,0.));
#7873=DIRECTION('ref_axis',(0.,0.,1.));
#7874=DIRECTION('center_axis',(0.,-1.,0.));
#7875=DIRECTION('ref_axis',(0.,0.,-1.));
#7876=DIRECTION('center_axis',(0.,1.,0.));
#7877=DIRECTION('ref_axis',(0.,0.,-1.));
#7878=DIRECTION('center_axis',(0.,-1.,0.));
#7879=DIRECTION('ref_axis',(0.,0.,1.));
#7880=DIRECTION('',(0.,1.,0.));
#7881=DIRECTION('center_axis',(0.,-1.,0.));
#7882=DIRECTION('ref_axis',(0.,0.,-1.));
#7883=DIRECTION('center_axis',(0.,-1.,0.));
#7884=DIRECTION('ref_axis',(0.,0.,1.));
#7885=DIRECTION('center_axis',(0.,-1.,0.));
#7886=DIRECTION('ref_axis',(0.,0.,-1.));
#7887=DIRECTION('center_axis',(0.,1.,0.));
#7888=DIRECTION('ref_axis',(1.,0.,0.));
#7889=DIRECTION('center_axis',(0.,1.,0.));
#7890=DIRECTION('ref_axis',(1.,0.,0.));
#7891=DIRECTION('center_axis',(0.,1.,0.));
#7892=DIRECTION('ref_axis',(1.,0.,0.));
#7893=DIRECTION('center_axis',(0.,1.,0.));
#7894=DIRECTION('ref_axis',(1.,0.,0.));
#7895=DIRECTION('center_axis',(0.,1.,0.));
#7896=DIRECTION('ref_axis',(1.,0.,0.));
#7897=DIRECTION('center_axis',(0.,1.,0.));
#7898=DIRECTION('ref_axis',(1.,0.,0.));
#7899=DIRECTION('center_axis',(0.,1.,0.));
#7900=DIRECTION('ref_axis',(1.,0.,0.));
#7901=DIRECTION('center_axis',(0.,1.,0.));
#7902=DIRECTION('ref_axis',(1.,0.,0.));
#7903=DIRECTION('center_axis',(0.,-1.,0.));
#7904=DIRECTION('ref_axis',(0.,0.,1.));
#7905=DIRECTION('',(0.,-1.,0.));
#7906=DIRECTION('center_axis',(0.,-1.,0.));
#7907=DIRECTION('ref_axis',(0.,0.,-1.));
#7908=DIRECTION('center_axis',(0.,-1.,0.));
#7909=DIRECTION('ref_axis',(0.,0.,1.));
#7910=DIRECTION('center_axis',(0.,-1.,0.));
#7911=DIRECTION('ref_axis',(0.,0.,-1.));
#7912=DIRECTION('center_axis',(0.,-1.,0.));
#7913=DIRECTION('ref_axis',(0.,0.,1.));
#7914=DIRECTION('',(0.,1.,0.));
#7915=DIRECTION('center_axis',(0.,-1.,0.));
#7916=DIRECTION('ref_axis',(0.,0.,-1.));
#7917=DIRECTION('center_axis',(0.,-1.,0.));
#7918=DIRECTION('ref_axis',(0.,0.,1.));
#7919=DIRECTION('center_axis',(0.,-1.,0.));
#7920=DIRECTION('ref_axis',(0.,0.,-1.));
#7921=DIRECTION('center_axis',(0.,-1.,0.));
#7922=DIRECTION('ref_axis',(0.,0.,1.));
#7923=DIRECTION('',(0.,-1.,0.));
#7924=DIRECTION('center_axis',(0.,-1.,0.));
#7925=DIRECTION('ref_axis',(0.,0.,-1.));
#7926=DIRECTION('center_axis',(0.,-1.,0.));
#7927=DIRECTION('ref_axis',(0.,0.,1.));
#7928=DIRECTION('center_axis',(0.,-1.,0.));
#7929=DIRECTION('ref_axis',(0.,0.,-1.));
#7930=DIRECTION('center_axis',(0.,1.,0.));
#7931=DIRECTION('ref_axis',(1.,0.,0.));
#7932=DIRECTION('center_axis',(0.,1.,0.));
#7933=DIRECTION('ref_axis',(1.,0.,0.));
#7934=DIRECTION('center_axis',(0.,1.,0.));
#7935=DIRECTION('ref_axis',(1.,0.,0.));
#7936=DIRECTION('center_axis',(0.,1.,0.));
#7937=DIRECTION('ref_axis',(1.,0.,0.));
#7938=DIRECTION('center_axis',(0.,1.,0.));
#7939=DIRECTION('ref_axis',(1.,0.,0.));
#7940=DIRECTION('center_axis',(0.,1.,0.));
#7941=DIRECTION('ref_axis',(1.,0.,0.));
#7942=DIRECTION('center_axis',(0.,1.,0.));
#7943=DIRECTION('ref_axis',(1.,0.,0.));
#7944=DIRECTION('center_axis',(0.,1.,0.));
#7945=DIRECTION('ref_axis',(1.,0.,0.));
#7946=DIRECTION('center_axis',(0.,-1.,0.));
#7947=DIRECTION('ref_axis',(0.,0.,1.));
#7948=DIRECTION('',(0.,1.,0.));
#7949=DIRECTION('center_axis',(0.,-1.,0.));
#7950=DIRECTION('ref_axis',(0.,0.,-1.));
#7951=DIRECTION('center_axis',(0.,-1.,0.));
#7952=DIRECTION('ref_axis',(0.,0.,1.));
#7953=DIRECTION('center_axis',(0.,-1.,0.));
#7954=DIRECTION('ref_axis',(0.,0.,-1.));
#7955=DIRECTION('center_axis',(0.,-1.,0.));
#7956=DIRECTION('ref_axis',(0.,0.,1.));
#7957=DIRECTION('',(0.,-1.,0.));
#7958=DIRECTION('center_axis',(1.,0.,0.));
#7959=DIRECTION('ref_axis',(0.,-1.,0.));
#7960=DIRECTION('',(1.,0.,0.));
#7961=DIRECTION('center_axis',(1.,0.,0.));
#7962=DIRECTION('ref_axis',(0.,-1.,0.));
#7963=DIRECTION('',(1.,0.,0.));
#7964=DIRECTION('center_axis',(0.,1.,0.));
#7965=DIRECTION('ref_axis',(1.,0.,0.));
#7966=DIRECTION('',(0.,1.,0.));
#7967=DIRECTION('center_axis',(0.,1.,0.));
#7968=DIRECTION('ref_axis',(1.,0.,0.));
#7969=DIRECTION('',(0.,1.,0.));
#7970=DIRECTION('center_axis',(0.,1.,0.));
#7971=DIRECTION('ref_axis',(1.,0.,0.));
#7972=DIRECTION('',(0.,1.,0.));
#7973=DIRECTION('center_axis',(0.,1.,0.));
#7974=DIRECTION('ref_axis',(1.,0.,0.));
#7975=DIRECTION('',(0.,1.,0.));
#7976=DIRECTION('center_axis',(0.,1.,0.));
#7977=DIRECTION('ref_axis',(1.,0.,0.));
#7978=DIRECTION('',(0.,1.,0.));
#7979=DIRECTION('center_axis',(0.,1.,0.));
#7980=DIRECTION('ref_axis',(1.,0.,0.));
#7981=DIRECTION('',(0.,1.,0.));
#7982=DIRECTION('center_axis',(0.,1.,0.));
#7983=DIRECTION('ref_axis',(1.,0.,0.));
#7984=DIRECTION('',(0.,1.,0.));
#7985=DIRECTION('center_axis',(0.,1.,0.));
#7986=DIRECTION('ref_axis',(1.,0.,0.));
#7987=DIRECTION('',(0.,1.,0.));
#10448=CARTESIAN_POINT('',(0.,0.,0.));
#10449=CARTESIAN_POINT('Origin',(0.,-9.5,0.));
#10450=CARTESIAN_POINT('',(6.12323399573677E-16,-9.5,-5.));
#10451=CARTESIAN_POINT('Origin',(0.,-9.5,0.));
#10452=CARTESIAN_POINT('',(3.06161699786838E-16,-9.5,-2.5));
#10453=CARTESIAN_POINT('Origin',(0.,-9.5,0.));
#10454=CARTESIAN_POINT('Origin',(0.,5.725,0.));
#10455=CARTESIAN_POINT('',(6.12323399573677E-16,-2.5,-5.));
#10456=CARTESIAN_POINT('',(6.12323399573677E-16,5.725,-5.));
#10457=CARTESIAN_POINT('Origin',(0.,-2.5,0.));
#10458=CARTESIAN_POINT('',(-5.,-7.25,0.));
#10459=CARTESIAN_POINT('',(-5.,-4.75,1.53080849893419E-16));
#10460=CARTESIAN_POINT('Ctrl Pts',(-5.,-7.25,-6.93889390390723E-17));
#10461=CARTESIAN_POINT('Ctrl Pts',(-5.,-7.25,-0.157664715929046));
#10462=CARTESIAN_POINT('Ctrl Pts',(-4.99179575122445,-7.21835421378757,
-0.325388319770619));
#10463=CARTESIAN_POINT('Ctrl Pts',(-4.96215629725421,-7.09057657413409,
-0.633172380752554));
#10464=CARTESIAN_POINT('Ctrl Pts',(-4.94111880834681,-6.99448091912696,
-0.773286033839411));
#10465=CARTESIAN_POINT('Ctrl Pts',(-4.90138825645426,-6.7732705681841,-0.994496384782273));
#10466=CARTESIAN_POINT('Ctrl Pts',(-4.88005597223663,-6.63316335628804,
-1.09057998139517));
#10467=CARTESIAN_POINT('Ctrl Pts',(-4.84973579332106,-6.32540213501313,
-1.21834881761244));
#10468=CARTESIAN_POINT('Ctrl Pts',(-4.84122918275927,-6.15768676334799,
-1.25));
#10469=CARTESIAN_POINT('Ctrl Pts',(-4.84122918275927,-5.84231323665201,
-1.25));
#10470=CARTESIAN_POINT('Ctrl Pts',(-4.84973579332106,-5.67459786498688,
-1.21834881761244));
#10471=CARTESIAN_POINT('Ctrl Pts',(-4.88005597223663,-5.36683664371196,
-1.09057998139517));
#10472=CARTESIAN_POINT('Ctrl Pts',(-4.90138825645426,-5.2267294318159,-0.994496384782273));
#10473=CARTESIAN_POINT('Ctrl Pts',(-4.94111880834681,-5.00551908087304,
-0.773286033839411));
#10474=CARTESIAN_POINT('Ctrl Pts',(-4.96215629725421,-4.90942342586591,
-0.633172380752555));
#10475=CARTESIAN_POINT('Ctrl Pts',(-4.99179575122445,-4.78164578621243,
-0.32538831977062));
#10476=CARTESIAN_POINT('Ctrl Pts',(-5.,-4.75,-0.157664715929046));
#10477=CARTESIAN_POINT('Ctrl Pts',(-5.,-4.75,3.46944695195361E-17));
#10478=CARTESIAN_POINT('Ctrl Pts',(-5.,-4.75,1.38777878078145E-16));
#10479=CARTESIAN_POINT('Ctrl Pts',(-5.,-4.75,0.157664715929046));
#10480=CARTESIAN_POINT('Ctrl Pts',(-4.99179575122445,-4.78164578621243,
0.32538831977062));
#10481=CARTESIAN_POINT('Ctrl Pts',(-4.96215629725421,-4.90942342586591,
0.633172380752555));
#10482=CARTESIAN_POINT('Ctrl Pts',(-4.94111880834681,-5.00551908087304,
0.773286033839411));
#10483=CARTESIAN_POINT('Ctrl Pts',(-4.90138825645426,-5.2267294318159,0.994496384782273));
#10484=CARTESIAN_POINT('Ctrl Pts',(-4.88005597223663,-5.36683664371196,
1.09057998139517));
#10485=CARTESIAN_POINT('Ctrl Pts',(-4.84973579332106,-5.67459786498688,
1.21834881761244));
#10486=CARTESIAN_POINT('Ctrl Pts',(-4.84122918275927,-5.84231323665201,
1.25));
#10487=CARTESIAN_POINT('Ctrl Pts',(-4.84122918275927,-6.,1.25));
#10488=CARTESIAN_POINT('Ctrl Pts',(-4.84122918275927,-6.15768676334799,
1.25));
#10489=CARTESIAN_POINT('Ctrl Pts',(-4.84973579332106,-6.32540213501313,
1.21834881761244));
#10490=CARTESIAN_POINT('Ctrl Pts',(-4.88005597223663,-6.63316335628804,
1.09057998139517));
#10491=CARTESIAN_POINT('Ctrl Pts',(-4.90138825645426,-6.7732705681841,0.994496384782273));
#10492=CARTESIAN_POINT('Ctrl Pts',(-4.94111880834681,-6.99448091912696,
0.773286033839411));
#10493=CARTESIAN_POINT('Ctrl Pts',(-4.96215629725421,-7.09057657413409,
0.633172380752555));
#10494=CARTESIAN_POINT('Ctrl Pts',(-4.99179575122445,-7.21835421378757,
0.32538831977062));
#10495=CARTESIAN_POINT('Ctrl Pts',(-5.,-7.25,0.157664715929046));
#10496=CARTESIAN_POINT('Ctrl Pts',(-5.,-7.25,-3.81639164714898E-16));
#10497=CARTESIAN_POINT('',(5.,-4.75,0.));
#10498=CARTESIAN_POINT('Ctrl Pts',(4.84122918275927,-6.,1.25));
#10499=CARTESIAN_POINT('Ctrl Pts',(4.84122918275927,-5.84231323665201,1.25));
#10500=CARTESIAN_POINT('Ctrl Pts',(4.84973579332106,-5.67459786498687,1.21834881761244));
#10501=CARTESIAN_POINT('Ctrl Pts',(4.88005597223663,-5.36683664371196,1.09057998139517));
#10502=CARTESIAN_POINT('Ctrl Pts',(4.90138825645426,-5.2267294318159,0.994496384782273));
#10503=CARTESIAN_POINT('Ctrl Pts',(4.94111880834681,-5.00551908087304,0.773286033839411));
#10504=CARTESIAN_POINT('Ctrl Pts',(4.96215629725421,-4.90942342586591,0.633172380752555));
#10505=CARTESIAN_POINT('Ctrl Pts',(4.99179575122445,-4.78164578621243,0.32538831977062));
#10506=CARTESIAN_POINT('Ctrl Pts',(5.,-4.75,0.157664715929046));
#10507=CARTESIAN_POINT('Ctrl Pts',(5.,-4.75,-0.157664715929046));
#10508=CARTESIAN_POINT('Ctrl Pts',(4.99179575122445,-4.78164578621243,-0.325388319770619));
#10509=CARTESIAN_POINT('Ctrl Pts',(4.96215629725421,-4.90942342586591,-0.633172380752555));
#10510=CARTESIAN_POINT('Ctrl Pts',(4.94111880834681,-5.00551908087304,-0.773286033839411));
#10511=CARTESIAN_POINT('Ctrl Pts',(4.90138825645426,-5.2267294318159,-0.994496384782273));
#10512=CARTESIAN_POINT('Ctrl Pts',(4.88005597223663,-5.36683664371196,-1.09057998139517));
#10513=CARTESIAN_POINT('Ctrl Pts',(4.84973579332106,-5.67459786498688,-1.21834881761244));
#10514=CARTESIAN_POINT('Ctrl Pts',(4.84122918275927,-5.84231323665201,-1.25));
#10515=CARTESIAN_POINT('Ctrl Pts',(4.84122918275927,-6.15768676334799,-1.25));
#10516=CARTESIAN_POINT('Ctrl Pts',(4.84973579332106,-6.32540213501313,-1.21834881761244));
#10517=CARTESIAN_POINT('Ctrl Pts',(4.88005597223663,-6.63316335628804,-1.09057998139517));
#10518=CARTESIAN_POINT('Ctrl Pts',(4.90138825645426,-6.7732705681841,-0.994496384782273));
#10519=CARTESIAN_POINT('Ctrl Pts',(4.94111880834681,-6.99448091912696,-0.773286033839411));
#10520=CARTESIAN_POINT('Ctrl Pts',(4.96215629725421,-7.09057657413409,-0.633172380752555));
#10521=CARTESIAN_POINT('Ctrl Pts',(4.99179575122445,-7.21835421378757,-0.32538831977062));
#10522=CARTESIAN_POINT('Ctrl Pts',(5.,-7.25,-0.157664715929046));
#10523=CARTESIAN_POINT('Ctrl Pts',(5.,-7.25,0.157664715929046));
#10524=CARTESIAN_POINT('Ctrl Pts',(4.99179575122445,-7.21835421378757,0.325388319770619));
#10525=CARTESIAN_POINT('Ctrl Pts',(4.96215629725421,-7.09057657413409,0.633172380752555));
#10526=CARTESIAN_POINT('Ctrl Pts',(4.94111880834681,-6.99448091912696,0.773286033839411));
#10527=CARTESIAN_POINT('Ctrl Pts',(4.90138825645426,-6.7732705681841,0.994496384782273));
#10528=CARTESIAN_POINT('Ctrl Pts',(4.88005597223663,-6.63316335628804,1.09057998139517));
#10529=CARTESIAN_POINT('Ctrl Pts',(4.84973579332106,-6.32540213501313,1.21834881761244));
#10530=CARTESIAN_POINT('Ctrl Pts',(4.84122918275927,-6.15768676334799,1.25));
#10531=CARTESIAN_POINT('Ctrl Pts',(4.84122918275927,-6.,1.25));
#10532=CARTESIAN_POINT('Origin',(0.,-2.5,0.));
#10533=CARTESIAN_POINT('',(4.28626379701574E-15,-2.5,-35.));
#10534=CARTESIAN_POINT('Origin',(0.,-2.5,0.));
#10535=CARTESIAN_POINT('',(-12.5,-2.5,-20.));
#10536=CARTESIAN_POINT('Origin',(0.,-2.5,-20.));
#10537=CARTESIAN_POINT('',(-12.5,-2.5,20.));
#10538=CARTESIAN_POINT('Origin',(0.,-2.5,20.));
#10539=CARTESIAN_POINT('',(7.5,-2.5,0.));
#10540=CARTESIAN_POINT('Origin',(20.,-2.5,0.));
#10541=CARTESIAN_POINT('',(-32.5,-2.5,0.));
#10542=CARTESIAN_POINT('Origin',(-20.,-2.5,0.));
#10543=CARTESIAN_POINT('',(13.67105307091,-2.5,-19.5));
#10544=CARTESIAN_POINT('Origin',(19.67105307091,-2.5,-19.5));
#10545=CARTESIAN_POINT('',(-25.67105307091,-2.5,-19.5));
#10546=CARTESIAN_POINT('Origin',(-19.67105307091,-2.5,-19.5));
#10547=CARTESIAN_POINT('',(13.67105307091,-2.5,19.5));
#10548=CARTESIAN_POINT('Origin',(19.67105307091,-2.5,19.5));
#10549=CARTESIAN_POINT('',(-25.67105307091,-2.5,19.5));
#10550=CARTESIAN_POINT('Origin',(-19.67105307091,-2.5,19.5));
#10551=CARTESIAN_POINT('Origin',(0.,5.725,0.));
#10552=CARTESIAN_POINT('',(4.28626379701574E-15,-5.,-35.));
#10553=CARTESIAN_POINT('',(4.28626379701574E-15,5.725,-35.));
#10554=CARTESIAN_POINT('Origin',(0.,-5.,0.));
#10555=CARTESIAN_POINT('Origin',(0.,-5.,0.));
#10556=CARTESIAN_POINT('',(4.89858719658941E-15,-5.,-40.));
#10557=CARTESIAN_POINT('Origin',(0.,-5.,0.));
#10558=CARTESIAN_POINT('Origin',(0.,5.725,0.));
#10559=CARTESIAN_POINT('',(4.89858719658941E-15,5.,-40.));
#10560=CARTESIAN_POINT('',(4.89858719658941E-15,5.725,-40.));
#10561=CARTESIAN_POINT('Origin',(0.,5.,0.));
#10562=CARTESIAN_POINT('Origin',(0.,5.,0.));
#10563=CARTESIAN_POINT('',(4.28626379701574E-15,5.,-35.));
#10564=CARTESIAN_POINT('Origin',(0.,5.,0.));
#10565=CARTESIAN_POINT('Origin',(0.,5.725,0.));
#10566=CARTESIAN_POINT('',(4.28626379701574E-15,2.5,-35.));
#10567=CARTESIAN_POINT('',(4.28626379701574E-15,5.725,-35.));
#10568=CARTESIAN_POINT('Origin',(0.,2.5,0.));
#10569=CARTESIAN_POINT('Origin',(0.,2.5,0.));
#10570=CARTESIAN_POINT('',(6.12323399573677E-16,2.5,-5.));
#10571=CARTESIAN_POINT('Origin',(0.,2.5,0.));
#10572=CARTESIAN_POINT('',(-12.5,2.5,-20.));
#10573=CARTESIAN_POINT('Origin',(0.,2.5,-20.));
#10574=CARTESIAN_POINT('',(-12.5,2.5,20.));
#10575=CARTESIAN_POINT('Origin',(0.,2.5,20.));
#10576=CARTESIAN_POINT('',(7.5,2.5,0.));
#10577=CARTESIAN_POINT('Origin',(20.,2.5,0.));
#10578=CARTESIAN_POINT('',(-32.5,2.5,0.));
#10579=CARTESIAN_POINT('Origin',(-20.,2.5,0.));
#10580=CARTESIAN_POINT('',(13.67105307091,2.5,-19.5));
#10581=CARTESIAN_POINT('Origin',(19.67105307091,2.5,-19.5));
#10582=CARTESIAN_POINT('',(-25.67105307091,2.5,-19.5));
#10583=CARTESIAN_POINT('Origin',(-19.67105307091,2.5,-19.5));
#10584=CARTESIAN_POINT('',(13.67105307091,2.5,19.5));
#10585=CARTESIAN_POINT('Origin',(19.67105307091,2.5,19.5));
#10586=CARTESIAN_POINT('',(-25.67105307091,2.5,19.5));
#10587=CARTESIAN_POINT('Origin',(-19.67105307091,2.5,19.5));
#10588=CARTESIAN_POINT('Origin',(0.,5.725,0.));
#10589=CARTESIAN_POINT('',(6.12323399573677E-16,5.,-5.));
#10590=CARTESIAN_POINT('',(6.12323399573677E-16,5.725,-5.));
#10591=CARTESIAN_POINT('Origin',(0.,5.,0.));
#10592=CARTESIAN_POINT('Origin',(0.,5.,0.));
#10593=CARTESIAN_POINT('',(3.06161699786838E-16,5.,-2.5));
#10594=CARTESIAN_POINT('Origin',(0.,5.,0.));
#10595=CARTESIAN_POINT('Origin',(0.,5.725,0.));
#10596=CARTESIAN_POINT('',(3.06161699786838E-16,5.725,-2.5));
#10597=CARTESIAN_POINT('',(-2.5,-4.75,0.));
#10598=CARTESIAN_POINT('Ctrl Pts',(-2.1650635094611,-6.,1.25));
#10599=CARTESIAN_POINT('Ctrl Pts',(-2.1650635094611,-5.83961866629939,1.25));
#10600=CARTESIAN_POINT('Ctrl Pts',(-2.18478179494117,-5.67107674842089,
1.21735698059595));
#10601=CARTESIAN_POINT('Ctrl Pts',(-2.25149501557585,-5.36427205061522,
1.08903588717028));
#10602=CARTESIAN_POINT('Ctrl Pts',(-2.29712558443605,-5.22567783219742,
0.993444785163793));
#10603=CARTESIAN_POINT('Ctrl Pts',(-2.37983326258812,-5.00685388429146,
0.774620837257829));
#10604=CARTESIAN_POINT('Ctrl Pts',(-2.42283105129935,-4.91104365009427,
0.635925947642968));
#10605=CARTESIAN_POINT('Ctrl Pts',(-2.48323996043832,-4.78254511766359,
0.328681344361069));
#10606=CARTESIAN_POINT('Ctrl Pts',(-2.5,-4.75,0.159944126385861));
#10607=CARTESIAN_POINT('Ctrl Pts',(-2.5,-4.75,-0.159944126385861));
#10608=CARTESIAN_POINT('Ctrl Pts',(-2.48323996043832,-4.78254511766359,
-0.328681344361069));
#10609=CARTESIAN_POINT('Ctrl Pts',(-2.42283105129935,-4.91104365009427,
-0.635925947642968));
#10610=CARTESIAN_POINT('Ctrl Pts',(-2.37983326258812,-5.00685388429146,
-0.774620837257828));
#10611=CARTESIAN_POINT('Ctrl Pts',(-2.29712558443605,-5.22567783219742,
-0.993444785163793));
#10612=CARTESIAN_POINT('Ctrl Pts',(-2.25149501557585,-5.36427205061522,
-1.08903588717028));
#10613=CARTESIAN_POINT('Ctrl Pts',(-2.18478179494117,-5.67107674842089,
-1.21735698059595));
#10614=CARTESIAN_POINT('Ctrl Pts',(-2.1650635094611,-5.83961866629939,-1.25));
#10615=CARTESIAN_POINT('Ctrl Pts',(-2.1650635094611,-6.16038133370061,-1.25));
#10616=CARTESIAN_POINT('Ctrl Pts',(-2.18478179494117,-6.32892325157911,
-1.21735698059595));
#10617=CARTESIAN_POINT('Ctrl Pts',(-2.25149501557585,-6.63572794938478,
-1.08903588717028));
#10618=CARTESIAN_POINT('Ctrl Pts',(-2.29712558443605,-6.77432216780258,
-0.993444785163793));
#10619=CARTESIAN_POINT('Ctrl Pts',(-2.37983326258812,-6.99314611570854,
-0.774620837257829));
#10620=CARTESIAN_POINT('Ctrl Pts',(-2.42283105129935,-7.08895634990573,
-0.635925947642969));
#10621=CARTESIAN_POINT('Ctrl Pts',(-2.48323996043832,-7.21745488233641,
-0.32868134436107));
#10622=CARTESIAN_POINT('Ctrl Pts',(-2.5,-7.25,-0.159944126385861));
#10623=CARTESIAN_POINT('Ctrl Pts',(-2.5,-7.25,0.159944126385861));
#10624=CARTESIAN_POINT('Ctrl Pts',(-2.48323996043832,-7.21745488233641,
0.328681344361069));
#10625=CARTESIAN_POINT('Ctrl Pts',(-2.42283105129935,-7.08895634990573,
0.635925947642968));
#10626=CARTESIAN_POINT('Ctrl Pts',(-2.37983326258812,-6.99314611570854,
0.774620837257828));
#10627=CARTESIAN_POINT('Ctrl Pts',(-2.29712558443605,-6.77432216780258,
0.993444785163793));
#10628=CARTESIAN_POINT('Ctrl Pts',(-2.25149501557585,-6.63572794938478,
1.08903588717028));
#10629=CARTESIAN_POINT('Ctrl Pts',(-2.18478179494117,-6.32892325157911,
1.21735698059595));
#10630=CARTESIAN_POINT('Ctrl Pts',(-2.1650635094611,-6.16038133370061,1.25));
#10631=CARTESIAN_POINT('Ctrl Pts',(-2.1650635094611,-6.,1.25));
#10632=CARTESIAN_POINT('',(2.5,-7.25,0.));
#10633=CARTESIAN_POINT('',(2.5,-4.75,1.45929363985782E-16));
#10634=CARTESIAN_POINT('Ctrl Pts',(2.5,-7.25,-2.77555756156289E-16));
#10635=CARTESIAN_POINT('Ctrl Pts',(2.5,-7.25,-0.159944126385861));
#10636=CARTESIAN_POINT('Ctrl Pts',(2.48323996043832,-7.21745488233641,-0.328681344361069));
#10637=CARTESIAN_POINT('Ctrl Pts',(2.42283105129935,-7.08895634990573,-0.635925947642968));
#10638=CARTESIAN_POINT('Ctrl Pts',(2.37983326258812,-6.99314611570854,-0.774620837257829));
#10639=CARTESIAN_POINT('Ctrl Pts',(2.29712558443605,-6.77432216780258,-0.993444785163793));
#10640=CARTESIAN_POINT('Ctrl Pts',(2.25149501557585,-6.63572794938478,-1.08903588717028));
#10641=CARTESIAN_POINT('Ctrl Pts',(2.18478179494117,-6.32892325157911,-1.21735698059595));
#10642=CARTESIAN_POINT('Ctrl Pts',(2.1650635094611,-6.16038133370061,-1.25));
#10643=CARTESIAN_POINT('Ctrl Pts',(2.1650635094611,-5.83961866629939,-1.25));
#10644=CARTESIAN_POINT('Ctrl Pts',(2.18478179494117,-5.67107674842089,-1.21735698059595));
#10645=CARTESIAN_POINT('Ctrl Pts',(2.25149501557585,-5.36427205061522,-1.08903588717028));
#10646=CARTESIAN_POINT('Ctrl Pts',(2.29712558443605,-5.22567783219742,-0.993444785163793));
#10647=CARTESIAN_POINT('Ctrl Pts',(2.37983326258812,-5.00685388429146,-0.774620837257828));
#10648=CARTESIAN_POINT('Ctrl Pts',(2.42283105129935,-4.91104365009427,-0.635925947642968));
#10649=CARTESIAN_POINT('Ctrl Pts',(2.48323996043832,-4.78254511766359,-0.328681344361069));
#10650=CARTESIAN_POINT('Ctrl Pts',(2.5,-4.75,-0.159944126385861));
#10651=CARTESIAN_POINT('Ctrl Pts',(2.5,-4.75,2.42861286636753E-16));
#10652=CARTESIAN_POINT('Ctrl Pts',(2.5,-4.75,1.38777878078145E-16));
#10653=CARTESIAN_POINT('Ctrl Pts',(2.5,-4.75,0.159944126385861));
#10654=CARTESIAN_POINT('Ctrl Pts',(2.48323996043832,-4.78254511766359,0.328681344361069));
#10655=CARTESIAN_POINT('Ctrl Pts',(2.42283105129935,-4.91104365009427,0.635925947642968));
#10656=CARTESIAN_POINT('Ctrl Pts',(2.37983326258812,-5.00685388429146,0.774620837257829));
#10657=CARTESIAN_POINT('Ctrl Pts',(2.29712558443605,-5.22567783219742,0.993444785163793));
#10658=CARTESIAN_POINT('Ctrl Pts',(2.25149501557585,-5.36427205061522,1.08903588717028));
#10659=CARTESIAN_POINT('Ctrl Pts',(2.18478179494117,-5.67107674842089,1.21735698059595));
#10660=CARTESIAN_POINT('Ctrl Pts',(2.1650635094611,-5.83961866629939,1.25));
#10661=CARTESIAN_POINT('Ctrl Pts',(2.1650635094611,-6.,1.25));
#10662=CARTESIAN_POINT('Ctrl Pts',(2.1650635094611,-6.16038133370061,1.25));
#10663=CARTESIAN_POINT('Ctrl Pts',(2.18478179494117,-6.32892325157911,1.21735698059595));
#10664=CARTESIAN_POINT('Ctrl Pts',(2.25149501557585,-6.63572794938478,1.08903588717028));
#10665=CARTESIAN_POINT('Ctrl Pts',(2.29712558443605,-6.77432216780258,0.993444785163793));
#10666=CARTESIAN_POINT('Ctrl Pts',(2.37983326258812,-6.99314611570854,0.774620837257828));
#10667=CARTESIAN_POINT('Ctrl Pts',(2.42283105129935,-7.08895634990573,0.635925947642969));
#10668=CARTESIAN_POINT('Ctrl Pts',(2.48323996043832,-7.21745488233641,0.328681344361069));
#10669=CARTESIAN_POINT('Ctrl Pts',(2.5,-7.25,0.159944126385861));
#10670=CARTESIAN_POINT('Ctrl Pts',(2.5,-7.25,-3.46944695195361E-16));
#10671=CARTESIAN_POINT('Origin',(-8.8,-6.,0.));
#10672=CARTESIAN_POINT('',(-8.8,-4.75,1.53080849893419E-16));
#10673=CARTESIAN_POINT('Origin',(-8.8,-6.,0.));
#10674=CARTESIAN_POINT('',(-8.8,-4.75,1.53080849893419E-16));
#10675=CARTESIAN_POINT('Origin',(0.,-11.6,-20.));
#10676=CARTESIAN_POINT('',(-12.5,-11.6,-20.));
#10677=CARTESIAN_POINT('Origin',(0.,-11.6,20.));
#10678=CARTESIAN_POINT('',(-12.5,-11.6,20.));
#10679=CARTESIAN_POINT('Origin',(20.,-11.6,0.));
#10680=CARTESIAN_POINT('',(7.5,-11.6,1.53080849893419E-15));
#10681=CARTESIAN_POINT('Origin',(-20.,-11.6,0.));
#10682=CARTESIAN_POINT('',(-32.5,-11.6,1.53080849893419E-15));
#10683=CARTESIAN_POINT('Origin',(19.67105307091,-11.6,-19.5));
#10684=CARTESIAN_POINT('',(13.67105307091,-11.6,-19.5));
#10685=CARTESIAN_POINT('Origin',(-19.67105307091,-11.6,-19.5));
#10686=CARTESIAN_POINT('',(-25.67105307091,-11.6,-19.5));
#10687=CARTESIAN_POINT('Origin',(19.67105307091,-11.6,19.5));
#10688=CARTESIAN_POINT('',(13.67105307091,-11.6,19.5));
#10689=CARTESIAN_POINT('Origin',(-19.67105307091,-11.6,19.5));
#10690=CARTESIAN_POINT('',(-25.67105307091,-11.6,19.5));
#17075=UNCERTAINTY_MEASURE_WITH_UNIT(LENGTH_MEASURE(0.01),#17114,
'DISTANCE_ACCURACY_VALUE',
'Maximum model space distance between geometric entities at asserted c
onnectivities');
#17090=UNCERTAINTY_MEASURE_WITH_UNIT(LENGTH_MEASURE(0.01),#17114,
'DISTANCE_ACCURACY_VALUE',
'Maximum model space distance between geometric entities at asserted c
onnectivities');
#17098=(
GEOMETRIC_REPRESENTATION_CONTEXT(3)
GLOBAL_UNCERTAINTY_ASSIGNED_CONTEXT((#17075))
GLOBAL_UNIT_ASSIGNED_CONTEXT((#17114,#17116,#17117))
REPRESENTATION_CONTEXT('','3D')
);
#17113=(
GEOMETRIC_REPRESENTATION_CONTEXT(3)
GLOBAL_UNCERTAINTY_ASSIGNED_CONTEXT((#17090))
GLOBAL_UNIT_ASSIGNED_CONTEXT((#17114,#17116,#17117))
REPRESENTATION_CONTEXT('','3D')
);
#17114=(
LENGTH_UNIT()
NAMED_UNIT(*)
SI_UNIT(.MILLI.,.METRE.)
);
#17116=(
NAMED_UNIT(*)
PLANE_ANGLE_UNIT()
SI_UNIT($,.RADIAN.)
);
#17117=(
NAMED_UNIT(*)
SI_UNIT($,.STERADIAN.)
SOLID_ANGLE_UNIT()
);
#17125=SHAPE_DEFINITION_REPRESENTATION(#17151,#17191);
#17151=PRODUCT_DEFINITION_SHAPE('',$,#17214);
#17191=SHAPE_REPRESENTATION('',(#6558),#17098);
#17206=PRODUCT_DEFINITION_CONTEXT('part definition',#17274,'design');
#17214=PRODUCT_DEFINITION('FLYWHEEL','FLYWHEEL',#17236,#17206);
#17236=PRODUCT_DEFINITION_FORMATION('',$,#17283);
#17274=APPLICATION_CONTEXT(
'Core Data for Automotive Mechanical Design Process');
#17275=PRODUCT_CONTEXT('part definition',#17274,'mechanical');
#17283=PRODUCT('FLYWHEEL','FLYWHEEL','NOT SPECIFIED',(#17275));
#17298=PRESENTATION_STYLE_ASSIGNMENT((#17299));
#17299=SURFACE_STYLE_USAGE(.BOTH.,#17300);
#17300=SURFACE_SIDE_STYLE('',(#17301));
#17301=SURFACE_STYLE_FILL_AREA(#17302);
#17302=FILL_AREA_STYLE('Steel - Satin',(#17303));
#17303=FILL_AREA_STYLE_COLOUR('Steel - Satin',#17304);
#17304=COLOUR_RGB('Steel - Satin', 0.09019608, 0.27058824, 0.51372549);
ENDSEC;
END-ISO-10303-21;
